ISO-10303-21;
HEADER;
/* Generated by software containing ST-Developer
 * from STEP Tools, Inc. (www.steptools.com) 
 */

FILE_DESCRIPTION(
/* description */ ('Four-bar parallelogram arm'),
/* implementation_level */ '2;1');

FILE_NAME(
/* name */ 'Bearing cap (3).step',
/* time_stamp */ '2026-10-28T03:24:55-07:00',
/* author */ (''),
/* organization */ (''),
/* preprocessor_version */ 'ST-DEVELOPER v20.2',
/* originating_system */ 'Autodesk Translation Framework v15.17.0.0',
/* authorisation */ '');

FILE_SCHEMA (('AUTOMOTIVE_DESIGN { 1 0 10303 214 3 1 1 }'));
ENDSEC;

DATA;
#10=MECHANICAL_DESIGN_GEOMETRIC_PRESENTATION_REPRESENTATION('',(#645),#14512);
#545=SHAPE_REPRESENTATION_RELATIONSHIP('SRR','None',#14767,#595);
#595=ADVANCED_BREP_SHAPE_REPRESENTATION('',(#702),#14482);
#645=STYLED_ITEM('',(#15087),#702);
#702=MANIFOLD_SOLID_BREP('Body1',#7350);
#861=FACE_BOUND('',#1942,.T.);
#862=FACE_BOUND('',#1943,.T.);
#863=FACE_BOUND('',#1944,.T.);
#864=FACE_BOUND('',#1945,.T.);
#865=FACE_BOUND('',#1946,.T.);
#866=FACE_BOUND('',#1948,.T.);
#867=FACE_BOUND('',#1949,.T.);
#868=FACE_BOUND('',#1950,.T.);
#869=FACE_BOUND('',#1951,.T.);
#870=FACE_BOUND('',#1952,.T.);
#1103=PLANE('',#8350);
#1104=PLANE('',#8351);
#1389=FACE_OUTER_BOUND('',#1935,.T.);
#1390=FACE_OUTER_BOUND('',#1936,.T.);
#1391=FACE_OUTER_BOUND('',#1937,.T.);
#1392=FACE_OUTER_BOUND('',#1938,.T.);
#1393=FACE_OUTER_BOUND('',#1939,.T.);
#1394=FACE_OUTER_BOUND('',#1940,.T.);
#1395=FACE_OUTER_BOUND('',#1941,.T.);
#1396=FACE_OUTER_BOUND('',#1947,.T.);
#1935=EDGE_LOOP('',(#5766,#5767,#5768,#5769));
#1936=EDGE_LOOP('',(#5770,#5771,#5772,#5773));
#1937=EDGE_LOOP('',(#5774,#5775,#5776,#5777));
#1938=EDGE_LOOP('',(#5778,#5779,#5780,#5781));
#1939=EDGE_LOOP('',(#5782,#5783,#5784,#5785));
#1940=EDGE_LOOP('',(#5786,#5787,#5788,#5789));
#1941=EDGE_LOOP('',(#5790));
#1942=EDGE_LOOP('',(#5791));
#1943=EDGE_LOOP('',(#5792));
#1944=EDGE_LOOP('',(#5793));
#1945=EDGE_LOOP('',(#5794));
#1946=EDGE_LOOP('',(#5795));
#1947=EDGE_LOOP('',(#5796));
#1948=EDGE_LOOP('',(#5797));
#1949=EDGE_LOOP('',(#5798));
#1950=EDGE_LOOP('',(#5799));
#1951=EDGE_LOOP('',(#5800));
#1952=EDGE_LOOP('',(#5801));
#2515=LINE('',#12895,#2909);
#2516=LINE('',#12901,#2910);
#2517=LINE('',#12907,#2911);
#2518=LINE('',#12913,#2912);
#2519=LINE('',#12919,#2913);
#2520=LINE('',#12925,#2914);
#2909=VECTOR('',#9965,0.225000000000001);
#2910=VECTOR('',#9972,0.225000000000001);
#2911=VECTOR('',#9979,0.225000000000001);
#2912=VECTOR('',#9986,0.225000000000001);
#2913=VECTOR('',#9993,1.02);
#2914=VECTOR('',#10000,2.2);
#3280=CIRCLE('',#8333,0.225000000000001);
#3281=CIRCLE('',#8334,0.225000000000001);
#3282=CIRCLE('',#8336,0.225000000000001);
#3283=CIRCLE('',#8337,0.225000000000001);
#3284=CIRCLE('',#8339,0.225000000000001);
#3285=CIRCLE('',#8340,0.225000000000001);
#3286=CIRCLE('',#8342,0.225000000000001);
#3287=CIRCLE('',#8343,0.225000000000001);
#3288=CIRCLE('',#8345,1.02);
#3289=CIRCLE('',#8346,1.02);
#3290=CIRCLE('',#8348,2.2);
#3291=CIRCLE('',#8349,2.2);
#3802=VERTEX_POINT('',#12892);
#3803=VERTEX_POINT('',#12894);
#3804=VERTEX_POINT('',#12898);
#3805=VERTEX_POINT('',#12900);
#3806=VERTEX_POINT('',#12904);
#3807=VERTEX_POINT('',#12906);
#3808=VERTEX_POINT('',#12910);
#3809=VERTEX_POINT('',#12912);
#3810=VERTEX_POINT('',#12916);
#3811=VERTEX_POINT('',#12918);
#3812=VERTEX_POINT('',#12922);
#3813=VERTEX_POINT('',#12924);
#4514=EDGE_CURVE('',#3802,#3802,#3280,.T.);
#4515=EDGE_CURVE('',#3802,#3803,#2515,.T.);
#4516=EDGE_CURVE('',#3803,#3803,#3281,.T.);
#4517=EDGE_CURVE('',#3804,#3804,#3282,.T.);
#4518=EDGE_CURVE('',#3804,#3805,#2516,.T.);
#4519=EDGE_CURVE('',#3805,#3805,#3283,.T.);
#4520=EDGE_CURVE('',#3806,#3806,#3284,.T.);
#4521=EDGE_CURVE('',#3806,#3807,#2517,.T.);
#4522=EDGE_CURVE('',#3807,#3807,#3285,.T.);
#4523=EDGE_CURVE('',#3808,#3808,#3286,.T.);
#4524=EDGE_CURVE('',#3808,#3809,#2518,.T.);
#4525=EDGE_CURVE('',#3809,#3809,#3287,.T.);
#4526=EDGE_CURVE('',#3810,#3810,#3288,.T.);
#4527=EDGE_CURVE('',#3810,#3811,#2519,.T.);
#4528=EDGE_CURVE('',#3811,#3811,#3289,.T.);
#4529=EDGE_CURVE('',#3812,#3812,#3290,.T.);
#4530=EDGE_CURVE('',#3812,#3813,#2520,.T.);
#4531=EDGE_CURVE('',#3813,#3813,#3291,.T.);
#5766=ORIENTED_EDGE('',*,*,#4514,.F.);
#5767=ORIENTED_EDGE('',*,*,#4515,.T.);
#5768=ORIENTED_EDGE('',*,*,#4516,.F.);
#5769=ORIENTED_EDGE('',*,*,#4515,.F.);
#5770=ORIENTED_EDGE('',*,*,#4517,.F.);
#5771=ORIENTED_EDGE('',*,*,#4518,.T.);
#5772=ORIENTED_EDGE('',*,*,#4519,.F.);
#5773=ORIENTED_EDGE('',*,*,#4518,.F.);
#5774=ORIENTED_EDGE('',*,*,#4520,.F.);
#5775=ORIENTED_EDGE('',*,*,#4521,.T.);
#5776=ORIENTED_EDGE('',*,*,#4522,.F.);
#5777=ORIENTED_EDGE('',*,*,#4521,.F.);
#5778=ORIENTED_EDGE('',*,*,#4523,.F.);
#5779=ORIENTED_EDGE('',*,*,#4524,.T.);
#5780=ORIENTED_EDGE('',*,*,#4525,.F.);
#5781=ORIENTED_EDGE('',*,*,#4524,.F.);
#5782=ORIENTED_EDGE('',*,*,#4526,.F.);
#5783=ORIENTED_EDGE('',*,*,#4527,.T.);
#5784=ORIENTED_EDGE('',*,*,#4528,.T.);
#5785=ORIENTED_EDGE('',*,*,#4527,.F.);
#5786=ORIENTED_EDGE('',*,*,#4529,.F.);
#5787=ORIENTED_EDGE('',*,*,#4530,.T.);
#5788=ORIENTED_EDGE('',*,*,#4531,.T.);
#5789=ORIENTED_EDGE('',*,*,#4530,.F.);
#5790=ORIENTED_EDGE('',*,*,#4529,.T.);
#5791=ORIENTED_EDGE('',*,*,#4526,.T.);
#5792=ORIENTED_EDGE('',*,*,#4525,.T.);
#5793=ORIENTED_EDGE('',*,*,#4522,.T.);
#5794=ORIENTED_EDGE('',*,*,#4519,.T.);
#5795=ORIENTED_EDGE('',*,*,#4516,.T.);
#5796=ORIENTED_EDGE('',*,*,#4531,.F.);
#5797=ORIENTED_EDGE('',*,*,#4528,.F.);
#5798=ORIENTED_EDGE('',*,*,#4523,.T.);
#5799=ORIENTED_EDGE('',*,*,#4520,.T.);
#5800=ORIENTED_EDGE('',*,*,#4517,.T.);
#5801=ORIENTED_EDGE('',*,*,#4514,.T.);
#6801=CYLINDRICAL_SURFACE('',#8332,0.225000000000001);
#6802=CYLINDRICAL_SURFACE('',#8335,0.225000000000001);
#6803=CYLINDRICAL_SURFACE('',#8338,0.225000000000001);
#6804=CYLINDRICAL_SURFACE('',#8341,0.225000000000001);
#6805=CYLINDRICAL_SURFACE('',#8344,1.02);
#6806=CYLINDRICAL_SURFACE('',#8347,2.2);
#7094=ADVANCED_FACE('',(#1389),#6801,.F.);
#7095=ADVANCED_FACE('',(#1390),#6802,.F.);
#7096=ADVANCED_FACE('',(#1391),#6803,.F.);
#7097=ADVANCED_FACE('',(#1392),#6804,.F.);
#7098=ADVANCED_FACE('',(#1393),#6805,.F.);
#7099=ADVANCED_FACE('',(#1394),#6806,.T.);
#7100=ADVANCED_FACE('',(#1395,#861,#862,#863,#864,#865),#1103,.T.);
#7101=ADVANCED_FACE('',(#1396,#866,#867,#868,#869,#870),#1104,.F.);
#7350=CLOSED_SHELL('',(#7094,#7095,#7096,#7097,#7098,#7099,#7100,#7101));
#8331=AXIS2_PLACEMENT_3D('',#12890,#9959,#9960);
#8332=AXIS2_PLACEMENT_3D('',#12891,#9961,#9962);
#8333=AXIS2_PLACEMENT_3D('',#12893,#9963,#9964);
#8334=AXIS2_PLACEMENT_3D('',#12896,#9966,#9967);
#8335=AXIS2_PLACEMENT_3D('',#12897,#9968,#9969);
#8336=AXIS2_PLACEMENT_3D('',#12899,#9970,#9971);
#8337=AXIS2_PLACEMENT_3D('',#12902,#9973,#9974);
#8338=AXIS2_PLACEMENT_3D('',#12903,#9975,#9976);
#8339=AXIS2_PLACEMENT_3D('',#12905,#9977,#9978);
#8340=AXIS2_PLACEMENT_3D('',#12908,#9980,#9981);
#8341=AXIS2_PLACEMENT_3D('',#12909,#9982,#9983);
#8342=AXIS2_PLACEMENT_3D('',#12911,#9984,#9985);
#8343=AXIS2_PLACEMENT_3D('',#12914,#9987,#9988);
#8344=AXIS2_PLACEMENT_3D('',#12915,#9989,#9990);
#8345=AXIS2_PLACEMENT_3D('',#12917,#9991,#9992);
#8346=AXIS2_PLACEMENT_3D('',#12920,#9994,#9995);
#8347=AXIS2_PLACEMENT_3D('',#12921,#9996,#9997);
#8348=AXIS2_PLACEMENT_3D('',#12923,#9998,#9999);
#8349=AXIS2_PLACEMENT_3D('',#12926,#10001,#10002);
#8350=AXIS2_PLACEMENT_3D('',#12927,#10003,#10004);
#8351=AXIS2_PLACEMENT_3D('',#12928,#10005,#10006);
#9959=DIRECTION('axis',(0.,0.,1.));
#9960=DIRECTION('refdir',(1.,0.,0.));
#9961=DIRECTION('center_axis',(0.,1.,0.));
#9962=DIRECTION('ref_axis',(1.,0.,0.));
#9963=DIRECTION('center_axis',(0.,1.,0.));
#9964=DIRECTION('ref_axis',(1.,0.,0.));
#9965=DIRECTION('',(0.,1.,0.));
#9966=DIRECTION('center_axis',(0.,-1.,0.));
#9967=DIRECTION('ref_axis',(1.,0.,0.));
#9968=DIRECTION('center_axis',(0.,1.,0.));
#9969=DIRECTION('ref_axis',(1.,0.,0.));
#9970=DIRECTION('center_axis',(0.,1.,0.));
#9971=DIRECTION('ref_axis',(1.,0.,0.));
#9972=DIRECTION('',(0.,1.,0.));
#9973=DIRECTION('center_axis',(0.,-1.,0.));
#9974=DIRECTION('ref_axis',(1.,0.,0.));
#9975=DIRECTION('center_axis',(0.,1.,0.));
#9976=DIRECTION('ref_axis',(1.,0.,0.));
#9977=DIRECTION('center_axis',(0.,1.,0.));
#9978=DIRECTION('ref_axis',(1.,0.,0.));
#9979=DIRECTION('',(0.,1.,0.));
#9980=DIRECTION('center_axis',(0.,-1.,0.));
#9981=DIRECTION('ref_axis',(1.,0.,0.));
#9982=DIRECTION('center_axis',(0.,1.,0.));
#9983=DIRECTION('ref_axis',(1.,0.,0.));
#9984=DIRECTION('center_axis',(0.,1.,0.));
#9985=DIRECTION('ref_axis',(1.,0.,0.));
#9986=DIRECTION('',(0.,1.,0.));
#9987=DIRECTION('center_axis',(0.,-1.,0.));
#9988=DIRECTION('ref_axis',(1.,0.,0.));
#9989=DIRECTION('center_axis',(0.,1.,0.));
#9990=DIRECTION('ref_axis',(1.,0.,0.));
#9991=DIRECTION('center_axis',(0.,-1.,0.));
#9992=DIRECTION('ref_axis',(1.,0.,0.));
#9993=DIRECTION('',(0.,-1.,0.));
#9994=DIRECTION('center_axis',(0.,-1.,0.));
#9995=DIRECTION('ref_axis',(1.,0.,0.));
#9996=DIRECTION('center_axis',(0.,1.,0.));
#9997=DIRECTION('ref_axis',(1.,0.,0.));
#9998=DIRECTION('center_axis',(0.,1.,0.));
#9999=DIRECTION('ref_axis',(1.,0.,0.));
#10000=DIRECTION('',(0.,-1.,0.));
#10001=DIRECTION('center_axis',(0.,1.,0.));
#10002=DIRECTION('ref_axis',(1.,0.,0.));
#10003=DIRECTION('center_axis',(0.,1.,0.));
#10004=DIRECTION('ref_axis',(1.,0.,0.));
#10005=DIRECTION('center_axis',(0.,1.,0.));
#10006=DIRECTION('ref_axis',(1.,0.,0.));
#12890=CARTESIAN_POINT('',(0.,0.,0.));
#12891=CARTESIAN_POINT('Origin',(18.7625631329235,0.95,6.76256313292354));
#12892=CARTESIAN_POINT('',(18.5375631329235,1.05,6.76256313292354));
#12893=CARTESIAN_POINT('Origin',(18.7625631329235,1.05,6.76256313292354));
#12894=CARTESIAN_POINT('',(18.5375631329235,1.4,6.76256313292354));
#12895=CARTESIAN_POINT('',(18.5375631329235,0.95,6.76256313292354));
#12896=CARTESIAN_POINT('Origin',(18.7625631329235,1.4,6.76256313292354));
#12897=CARTESIAN_POINT('Origin',(18.7625631329235,0.95,9.23743686707646));
#12898=CARTESIAN_POINT('',(18.5375631329235,1.05,9.23743686707646));
#12899=CARTESIAN_POINT('Origin',(18.7625631329235,1.05,9.23743686707646));
#12900=CARTESIAN_POINT('',(18.5375631329235,1.4,9.23743686707646));
#12901=CARTESIAN_POINT('',(18.5375631329235,0.95,9.23743686707646));
#12902=CARTESIAN_POINT('Origin',(18.7625631329235,1.4,9.23743686707646));
#12903=CARTESIAN_POINT('Origin',(21.2374368670765,0.95,9.23743686707646));
#12904=CARTESIAN_POINT('',(21.0124368670765,1.05,9.23743686707646));
#12905=CARTESIAN_POINT('Origin',(21.2374368670765,1.05,9.23743686707646));
#12906=CARTESIAN_POINT('',(21.0124368670765,1.4,9.23743686707646));
#12907=CARTESIAN_POINT('',(21.0124368670765,0.95,9.23743686707646));
#12908=CARTESIAN_POINT('Origin',(21.2374368670765,1.4,9.23743686707646));
#12909=CARTESIAN_POINT('Origin',(21.2374368670765,0.95,6.76256313292354));
#12910=CARTESIAN_POINT('',(21.0124368670765,1.05,6.76256313292354));
#12911=CARTESIAN_POINT('Origin',(21.2374368670765,1.05,6.76256313292354));
#12912=CARTESIAN_POINT('',(21.0124368670765,1.4,6.76256313292354));
#12913=CARTESIAN_POINT('',(21.0124368670765,0.95,6.76256313292354));
#12914=CARTESIAN_POINT('Origin',(21.2374368670765,1.4,6.76256313292354));
#12915=CARTESIAN_POINT('Origin',(20.,1.05,8.));
#12916=CARTESIAN_POINT('',(18.98,1.4,8.));
#12917=CARTESIAN_POINT('Origin',(20.,1.4,8.));
#12918=CARTESIAN_POINT('',(18.98,1.05,8.));
#12919=CARTESIAN_POINT('',(18.98,1.05,8.));
#12920=CARTESIAN_POINT('Origin',(20.,1.05,8.));
#12921=CARTESIAN_POINT('Origin',(20.,1.05,8.));
#12922=CARTESIAN_POINT('',(17.8,1.4,8.));
#12923=CARTESIAN_POINT('Origin',(20.,1.4,8.));
#12924=CARTESIAN_POINT('',(17.8,1.05,8.));
#12925=CARTESIAN_POINT('',(17.8,1.05,8.));
#12926=CARTESIAN_POINT('Origin',(20.,1.05,8.));
#12927=CARTESIAN_POINT('Origin',(20.,1.4,8.));
#12928=CARTESIAN_POINT('Origin',(20.,1.05,8.));
#14425=UNCERTAINTY_MEASURE_WITH_UNIT(LENGTH_MEASURE(0.001),#14513,
'DISTANCE_ACCURACY_VALUE',
'Maximum model space distance between geometric entities at asserted c
onnectivities');
#14455=UNCERTAINTY_MEASURE_WITH_UNIT(LENGTH_MEASURE(0.001),#14513,
'DISTANCE_ACCURACY_VALUE',
'Maximum model space distance between geometric entities at asserted c
onnectivities');
#14482=(
GEOMETRIC_REPRESENTATION_CONTEXT(3)
GLOBAL_UNCERTAINTY_ASSIGNED_CONTEXT((#14425))
GLOBAL_UNIT_ASSIGNED_CONTEXT((#14513,#14515,#14516))
REPRESENTATION_CONTEXT('','3D')
);
#14512=(
GEOMETRIC_REPRESENTATION_CONTEXT(3)
GLOBAL_UNCERTAINTY_ASSIGNED_CONTEXT((#14455))
GLOBAL_UNIT_ASSIGNED_CONTEXT((#14513,#14515,#14516))
REPRESENTATION_CONTEXT('','3D')
);
#14513=(
LENGTH_UNIT()
NAMED_UNIT(*)
SI_UNIT(.CENTI.,.METRE.)
);
#14515=(
NAMED_UNIT(*)
PLANE_ANGLE_UNIT()
SI_UNIT($,.RADIAN.)
);
#14516=(
NAMED_UNIT(*)
SI_UNIT($,.STERADIAN.)
SOLID_ANGLE_UNIT()
);
#14543=SHAPE_DEFINITION_REPRESENTATION(#14599,#14767);
#14599=PRODUCT_DEFINITION_SHAPE('',$,#14824);
#14767=SHAPE_REPRESENTATION('',(#8331),#14482);
#14797=PRODUCT_DEFINITION_CONTEXT('part definition',#14967,'design');
#14824=PRODUCT_DEFINITION('Bearing cap (3)','Bearing cap (3)',#14880,#14797);
#14880=PRODUCT_DEFINITION_FORMATION('',$,#14995);
#14967=APPLICATION_CONTEXT(
'Core Data for Automotive Mechanical Design Process');
#14968=PRODUCT_CONTEXT('part definition',#14967,'mechanical');
#14995=PRODUCT('Bearing cap (3)','Bearing cap (3)','Bearing cap (3)',(#14968));
#15081=COLOUR_RGB('Grey',0.48,0.52,0.57);
#15082=FILL_AREA_STYLE_COLOUR('',#15081);
#15083=FILL_AREA_STYLE('',(#15082));
#15084=SURFACE_STYLE_FILL_AREA(#15083);
#15085=SURFACE_SIDE_STYLE('',(#15084));
#15086=SURFACE_STYLE_USAGE(.BOTH.,#15085);
#15087=PRESENTATION_STYLE_ASSIGNMENT((#15086));
ENDSEC;
END-ISO-10303-21;
